ISO-10303-21;
HEADER;
/* Generated by software containing ST-Developer
 * from STEP Tools, Inc. (www.steptools.com) 
 */

FILE_DESCRIPTION(
/* description */ ('Worm-less right-angle friction wheel drive'),
/* implementation_level */ '2;1');

FILE_NAME(
/* name */ 'Cap Screw - M6x25.step',
/* time_stamp */ '2026-10-28T03:22:36-07:00',
/* author */ (''),
/* organization */ (''),
/* preprocessor_version */ 'ST-DEVELOPER v20.2',
/* originating_system */ 'Autodesk Translation Framework v15.17.0.0',
/* authorisation */ '');

FILE_SCHEMA (('AUTOMOTIVE_DESIGN { 1 0 10303 214 3 1 1 }'));
ENDSEC;

DATA;
#10=MECHANICAL_DESIGN_GEOMETRIC_PRESENTATION_REPRESENTATION('',(#648),#17046);
#453=ORIENTED_CLOSED_SHELL('',*,#8206,.F.);
#466=CONICAL_SURFACE('',#9416,0.475,0.785398163397449);
#467=CONICAL_SURFACE('',#9420,0.485,0.785398163397448);
#468=CONICAL_SURFACE('',#9424,0.31,0.463647609000806);
#469=CONICAL_SURFACE('',#9428,0.27,0.785398163397448);
#479=BREP_WITH_VOIDS('Body1',#8205,(#453));
#547=SHAPE_REPRESENTATION_RELATIONSHIP('SRR','None',#17291,#594);
#594=ADVANCED_BREP_SHAPE_REPRESENTATION('',(#479),#17027);
#648=STYLED_ITEM('',(#17598),#479);
#916=FACE_BOUND('',#2195,.T.);
#1106=PLANE('',#9414);
#1107=PLANE('',#9422);
#1108=PLANE('',#9430);
#1109=PLANE('',#9431);
#1110=PLANE('',#9432);
#1111=PLANE('',#9433);
#1112=PLANE('',#9434);
#1113=PLANE('',#9435);
#1114=PLANE('',#9436);
#1115=PLANE('',#9437);
#1116=PLANE('',#9438);
#1523=FACE_OUTER_BOUND('',#2190,.T.);
#1524=FACE_OUTER_BOUND('',#2191,.T.);
#1525=FACE_OUTER_BOUND('',#2192,.T.);
#1526=FACE_OUTER_BOUND('',#2193,.T.);
#1527=FACE_OUTER_BOUND('',#2194,.T.);
#1528=FACE_OUTER_BOUND('',#2196,.T.);
#1529=FACE_OUTER_BOUND('',#2197,.T.);
#1530=FACE_OUTER_BOUND('',#2198,.T.);
#1531=FACE_OUTER_BOUND('',#2199,.T.);
#1532=FACE_OUTER_BOUND('',#2200,.T.);
#1533=FACE_OUTER_BOUND('',#2201,.T.);
#1534=FACE_OUTER_BOUND('',#2202,.T.);
#1535=FACE_OUTER_BOUND('',#2203,.T.);
#1536=FACE_OUTER_BOUND('',#2204,.T.);
#1537=FACE_OUTER_BOUND('',#2205,.T.);
#1538=FACE_OUTER_BOUND('',#2206,.T.);
#1539=FACE_OUTER_BOUND('',#2207,.T.);
#2190=EDGE_LOOP('',(#6924));
#2191=EDGE_LOOP('',(#6925,#6926,#6927,#6928));
#2192=EDGE_LOOP('',(#6929,#6930,#6931,#6932));
#2193=EDGE_LOOP('',(#6933,#6934,#6935,#6936));
#2194=EDGE_LOOP('',(#6937));
#2195=EDGE_LOOP('',(#6938));
#2196=EDGE_LOOP('',(#6939,#6940,#6941,#6942));
#2197=EDGE_LOOP('',(#6943,#6944,#6945,#6946));
#2198=EDGE_LOOP('',(#6947,#6948,#6949,#6950));
#2199=EDGE_LOOP('',(#6951));
#2200=EDGE_LOOP('',(#6952,#6953,#6954,#6955));
#2201=EDGE_LOOP('',(#6956,#6957,#6958,#6959));
#2202=EDGE_LOOP('',(#6960,#6961,#6962,#6963));
#2203=EDGE_LOOP('',(#6964,#6965,#6966,#6967));
#2204=EDGE_LOOP('',(#6968,#6969,#6970,#6971));
#2205=EDGE_LOOP('',(#6972,#6973,#6974,#6975));
#2206=EDGE_LOOP('',(#6976,#6977,#6978,#6979,#6980,#6981));
#2207=EDGE_LOOP('',(#6982,#6983,#6984,#6985,#6986,#6987));
#2736=LINE('',#15993,#3276);
#2737=LINE('',#15997,#3277);
#2738=LINE('',#16001,#3278);
#2739=LINE('',#16008,#3279);
#2740=LINE('',#16012,#3280);
#2741=LINE('',#16016,#3281);
#2742=LINE('',#16021,#3282);
#2743=LINE('',#16023,#3283);
#2744=LINE('',#16025,#3284);
#2745=LINE('',#16026,#3285);
#2746=LINE('',#16029,#3286);
#2747=LINE('',#16031,#3287);
#2748=LINE('',#16032,#3288);
#2749=LINE('',#16035,#3289);
#2750=LINE('',#16037,#3290);
#2751=LINE('',#16038,#3291);
#2752=LINE('',#16041,#3292);
#2753=LINE('',#16043,#3293);
#2754=LINE('',#16044,#3294);
#2755=LINE('',#16047,#3295);
#2756=LINE('',#16049,#3296);
#2757=LINE('',#16050,#3297);
#2758=LINE('',#16052,#3298);
#2759=LINE('',#16053,#3299);
#3276=VECTOR('',#11484,0.475);
#3277=VECTOR('',#11489,0.5);
#3278=VECTOR('',#11494,0.485);
#3279=VECTOR('',#11503,0.31);
#3280=VECTOR('',#11508,0.3);
#3281=VECTOR('',#11513,0.27);
#3282=VECTOR('',#11518,1.);
#3283=VECTOR('',#11519,1.);
#3284=VECTOR('',#11520,1.);
#3285=VECTOR('',#11521,1.);
#3286=VECTOR('',#11524,1.);
#3287=VECTOR('',#11525,1.);
#3288=VECTOR('',#11526,1.);
#3289=VECTOR('',#11529,1.);
#3290=VECTOR('',#11530,1.);
#3291=VECTOR('',#11531,1.);
#3292=VECTOR('',#11534,1.);
#3293=VECTOR('',#11535,1.);
#3294=VECTOR('',#11536,1.);
#3295=VECTOR('',#11539,1.);
#3296=VECTOR('',#11540,1.);
#3297=VECTOR('',#11541,1.);
#3298=VECTOR('',#11544,1.);
#3299=VECTOR('',#11545,1.);
#3777=CIRCLE('',#9415,0.45);
#3778=CIRCLE('',#9417,0.5);
#3779=CIRCLE('',#9419,0.5);
#3780=CIRCLE('',#9421,0.47);
#3781=CIRCLE('',#9423,0.32);
#3782=CIRCLE('',#9425,0.2942);
#3783=CIRCLE('',#9427,0.2942);
#3784=CIRCLE('',#9429,0.24);
#4338=VERTEX_POINT('',#15988);
#4339=VERTEX_POINT('',#15991);
#4340=VERTEX_POINT('',#15995);
#4341=VERTEX_POINT('',#15999);
#4342=VERTEX_POINT('',#16003);
#4343=VERTEX_POINT('',#16006);
#4344=VERTEX_POINT('',#16010);
#4345=VERTEX_POINT('',#16014);
#4346=VERTEX_POINT('',#16019);
#4347=VERTEX_POINT('',#16020);
#4348=VERTEX_POINT('',#16022);
#4349=VERTEX_POINT('',#16024);
#4350=VERTEX_POINT('',#16028);
#4351=VERTEX_POINT('',#16030);
#4352=VERTEX_POINT('',#16034);
#4353=VERTEX_POINT('',#16036);
#4354=VERTEX_POINT('',#16040);
#4355=VERTEX_POINT('',#16042);
#4356=VERTEX_POINT('',#16046);
#4357=VERTEX_POINT('',#16048);
#5231=EDGE_CURVE('',#4338,#4338,#3777,.T.);
#5232=EDGE_CURVE('',#4339,#4339,#3778,.T.);
#5233=EDGE_CURVE('',#4339,#4338,#2736,.T.);
#5234=EDGE_CURVE('',#4340,#4340,#3779,.T.);
#5235=EDGE_CURVE('',#4340,#4339,#2737,.T.);
#5236=EDGE_CURVE('',#4341,#4341,#3780,.T.);
#5237=EDGE_CURVE('',#4341,#4340,#2738,.T.);
#5238=EDGE_CURVE('',#4342,#4342,#3781,.T.);
#5239=EDGE_CURVE('',#4343,#4343,#3782,.F.);
#5240=EDGE_CURVE('',#4343,#4342,#2739,.T.);
#5241=EDGE_CURVE('',#4344,#4344,#3783,.F.);
#5242=EDGE_CURVE('',#4344,#4343,#2740,.T.);
#5243=EDGE_CURVE('',#4345,#4345,#3784,.T.);
#5244=EDGE_CURVE('',#4345,#4344,#2741,.T.);
#5245=EDGE_CURVE('',#4346,#4347,#2742,.T.);
#5246=EDGE_CURVE('',#4347,#4348,#2743,.T.);
#5247=EDGE_CURVE('',#4348,#4349,#2744,.T.);
#5248=EDGE_CURVE('',#4346,#4349,#2745,.T.);
#5249=EDGE_CURVE('',#4347,#4350,#2746,.T.);
#5250=EDGE_CURVE('',#4350,#4351,#2747,.T.);
#5251=EDGE_CURVE('',#4351,#4348,#2748,.T.);
#5252=EDGE_CURVE('',#4350,#4352,#2749,.T.);
#5253=EDGE_CURVE('',#4352,#4353,#2750,.T.);
#5254=EDGE_CURVE('',#4353,#4351,#2751,.T.);
#5255=EDGE_CURVE('',#4352,#4354,#2752,.T.);
#5256=EDGE_CURVE('',#4354,#4355,#2753,.T.);
#5257=EDGE_CURVE('',#4355,#4353,#2754,.T.);
#5258=EDGE_CURVE('',#4354,#4356,#2755,.T.);
#5259=EDGE_CURVE('',#4356,#4357,#2756,.T.);
#5260=EDGE_CURVE('',#4357,#4355,#2757,.T.);
#5261=EDGE_CURVE('',#4356,#4346,#2758,.T.);
#5262=EDGE_CURVE('',#4349,#4357,#2759,.T.);
#6924=ORIENTED_EDGE('',*,*,#5231,.F.);
#6925=ORIENTED_EDGE('',*,*,#5232,.F.);
#6926=ORIENTED_EDGE('',*,*,#5233,.T.);
#6927=ORIENTED_EDGE('',*,*,#5231,.T.);
#6928=ORIENTED_EDGE('',*,*,#5233,.F.);
#6929=ORIENTED_EDGE('',*,*,#5234,.F.);
#6930=ORIENTED_EDGE('',*,*,#5235,.T.);
#6931=ORIENTED_EDGE('',*,*,#5232,.T.);
#6932=ORIENTED_EDGE('',*,*,#5235,.F.);
#6933=ORIENTED_EDGE('',*,*,#5236,.F.);
#6934=ORIENTED_EDGE('',*,*,#5237,.T.);
#6935=ORIENTED_EDGE('',*,*,#5234,.T.);
#6936=ORIENTED_EDGE('',*,*,#5237,.F.);
#6937=ORIENTED_EDGE('',*,*,#5236,.T.);
#6938=ORIENTED_EDGE('',*,*,#5238,.F.);
#6939=ORIENTED_EDGE('',*,*,#5239,.F.);
#6940=ORIENTED_EDGE('',*,*,#5240,.T.);
#6941=ORIENTED_EDGE('',*,*,#5238,.T.);
#6942=ORIENTED_EDGE('',*,*,#5240,.F.);
#6943=ORIENTED_EDGE('',*,*,#5241,.F.);
#6944=ORIENTED_EDGE('',*,*,#5242,.T.);
#6945=ORIENTED_EDGE('',*,*,#5239,.T.);
#6946=ORIENTED_EDGE('',*,*,#5242,.F.);
#6947=ORIENTED_EDGE('',*,*,#5243,.F.);
#6948=ORIENTED_EDGE('',*,*,#5244,.T.);
#6949=ORIENTED_EDGE('',*,*,#5241,.T.);
#6950=ORIENTED_EDGE('',*,*,#5244,.F.);
#6951=ORIENTED_EDGE('',*,*,#5243,.T.);
#6952=ORIENTED_EDGE('',*,*,#5245,.T.);
#6953=ORIENTED_EDGE('',*,*,#5246,.T.);
#6954=ORIENTED_EDGE('',*,*,#5247,.T.);
#6955=ORIENTED_EDGE('',*,*,#5248,.F.);
#6956=ORIENTED_EDGE('',*,*,#5249,.T.);
#6957=ORIENTED_EDGE('',*,*,#5250,.T.);
#6958=ORIENTED_EDGE('',*,*,#5251,.T.);
#6959=ORIENTED_EDGE('',*,*,#5246,.F.);
#6960=ORIENTED_EDGE('',*,*,#5252,.T.);
#6961=ORIENTED_EDGE('',*,*,#5253,.T.);
#6962=ORIENTED_EDGE('',*,*,#5254,.T.);
#6963=ORIENTED_EDGE('',*,*,#5250,.F.);
#6964=ORIENTED_EDGE('',*,*,#5255,.T.);
#6965=ORIENTED_EDGE('',*,*,#5256,.T.);
#6966=ORIENTED_EDGE('',*,*,#5257,.T.);
#6967=ORIENTED_EDGE('',*,*,#5253,.F.);
#6968=ORIENTED_EDGE('',*,*,#5258,.T.);
#6969=ORIENTED_EDGE('',*,*,#5259,.T.);
#6970=ORIENTED_EDGE('',*,*,#5260,.T.);
#6971=ORIENTED_EDGE('',*,*,#5256,.F.);
#6972=ORIENTED_EDGE('',*,*,#5261,.T.);
#6973=ORIENTED_EDGE('',*,*,#5248,.T.);
#6974=ORIENTED_EDGE('',*,*,#5262,.T.);
#6975=ORIENTED_EDGE('',*,*,#5259,.F.);
#6976=ORIENTED_EDGE('',*,*,#5261,.F.);
#6977=ORIENTED_EDGE('',*,*,#5258,.F.);
#6978=ORIENTED_EDGE('',*,*,#5255,.F.);
#6979=ORIENTED_EDGE('',*,*,#5252,.F.);
#6980=ORIENTED_EDGE('',*,*,#5249,.F.);
#6981=ORIENTED_EDGE('',*,*,#5245,.F.);
#6982=ORIENTED_EDGE('',*,*,#5262,.F.);
#6983=ORIENTED_EDGE('',*,*,#5247,.F.);
#6984=ORIENTED_EDGE('',*,*,#5251,.F.);
#6985=ORIENTED_EDGE('',*,*,#5254,.F.);
#6986=ORIENTED_EDGE('',*,*,#5257,.F.);
#6987=ORIENTED_EDGE('',*,*,#5260,.F.);
#7662=CYLINDRICAL_SURFACE('',#9418,0.5);
#7663=CYLINDRICAL_SURFACE('',#9426,0.2942);
#8015=ADVANCED_FACE('',(#1523),#1106,.T.);
#8016=ADVANCED_FACE('',(#1524),#466,.T.);
#8017=ADVANCED_FACE('',(#1525),#7662,.T.);
#8018=ADVANCED_FACE('',(#1526),#467,.T.);
#8019=ADVANCED_FACE('',(#1527,#916),#1107,.T.);
#8020=ADVANCED_FACE('',(#1528),#468,.T.);
#8021=ADVANCED_FACE('',(#1529),#7663,.T.);
#8022=ADVANCED_FACE('',(#1530),#469,.T.);
#8023=ADVANCED_FACE('',(#1531),#1108,.T.);
#8024=ADVANCED_FACE('',(#1532),#1109,.F.);
#8025=ADVANCED_FACE('',(#1533),#1110,.F.);
#8026=ADVANCED_FACE('',(#1534),#1111,.F.);
#8027=ADVANCED_FACE('',(#1535),#1112,.F.);
#8028=ADVANCED_FACE('',(#1536),#1113,.F.);
#8029=ADVANCED_FACE('',(#1537),#1114,.F.);
#8030=ADVANCED_FACE('',(#1538),#1115,.F.);
#8031=ADVANCED_FACE('',(#1539),#1116,.F.);
#8205=CLOSED_SHELL('',(#8015,#8016,#8017,#8018,#8019,#8020,#8021,#8022,
#8023));
#8206=CLOSED_SHELL('',(#8024,#8025,#8026,#8027,#8028,#8029,#8030,#8031));
#9413=AXIS2_PLACEMENT_3D('',#15986,#11474,#11475);
#9414=AXIS2_PLACEMENT_3D('',#15987,#11476,#11477);
#9415=AXIS2_PLACEMENT_3D('',#15989,#11478,#11479);
#9416=AXIS2_PLACEMENT_3D('',#15990,#11480,#11481);
#9417=AXIS2_PLACEMENT_3D('',#15992,#11482,#11483);
#9418=AXIS2_PLACEMENT_3D('',#15994,#11485,#11486);
#9419=AXIS2_PLACEMENT_3D('',#15996,#11487,#11488);
#9420=AXIS2_PLACEMENT_3D('',#15998,#11490,#11491);
#9421=AXIS2_PLACEMENT_3D('',#16000,#11492,#11493);
#9422=AXIS2_PLACEMENT_3D('',#16002,#11495,#11496);
#9423=AXIS2_PLACEMENT_3D('',#16004,#11497,#11498);
#9424=AXIS2_PLACEMENT_3D('',#16005,#11499,#11500);
#9425=AXIS2_PLACEMENT_3D('',#16007,#11501,#11502);
#9426=AXIS2_PLACEMENT_3D('',#16009,#11504,#11505);
#9427=AXIS2_PLACEMENT_3D('',#16011,#11506,#11507);
#9428=AXIS2_PLACEMENT_3D('',#16013,#11509,#11510);
#9429=AXIS2_PLACEMENT_3D('',#16015,#11511,#11512);
#9430=AXIS2_PLACEMENT_3D('',#16017,#11514,#11515);
#9431=AXIS2_PLACEMENT_3D('',#16018,#11516,#11517);
#9432=AXIS2_PLACEMENT_3D('',#16027,#11522,#11523);
#9433=AXIS2_PLACEMENT_3D('',#16033,#11527,#11528);
#9434=AXIS2_PLACEMENT_3D('',#16039,#11532,#11533);
#9435=AXIS2_PLACEMENT_3D('',#16045,#11537,#11538);
#9436=AXIS2_PLACEMENT_3D('',#16051,#11542,#11543);
#9437=AXIS2_PLACEMENT_3D('',#16054,#11546,#11547);
#9438=AXIS2_PLACEMENT_3D('',#16055,#11548,#11549);
#11474=DIRECTION('axis',(0.,0.,1.));
#11475=DIRECTION('refdir',(1.,0.,0.));
#11476=DIRECTION('center_axis',(0.,1.,0.));
#11477=DIRECTION('ref_axis',(0.,0.,1.));
#11478=DIRECTION('center_axis',(0.,-1.,0.));
#11479=DIRECTION('ref_axis',(1.,0.,0.));
#11480=DIRECTION('center_axis',(0.,-1.,0.));
#11481=DIRECTION('ref_axis',(1.,0.,0.));
#11482=DIRECTION('center_axis',(0.,-1.,0.));
#11483=DIRECTION('ref_axis',(1.,0.,0.));
#11484=DIRECTION('',(0.707106781186548,0.707106781186547,8.65956056235494E-17));
#11485=DIRECTION('center_axis',(0.,-1.,0.));
#11486=DIRECTION('ref_axis',(1.,0.,0.));
#11487=DIRECTION('center_axis',(0.,-1.,0.));
#11488=DIRECTION('ref_axis',(1.,0.,0.));
#11489=DIRECTION('',(0.,1.,0.));
#11490=DIRECTION('center_axis',(0.,1.,0.));
#11491=DIRECTION('ref_axis',(1.,0.,0.));
#11492=DIRECTION('center_axis',(0.,-1.,0.));
#11493=DIRECTION('ref_axis',(1.,0.,0.));
#11494=DIRECTION('',(-0.707106781186547,0.707106781186548,-8.65956056235493E-17));
#11495=DIRECTION('center_axis',(0.,-1.,0.));
#11496=DIRECTION('ref_axis',(0.,0.,-1.));
#11497=DIRECTION('center_axis',(0.,-1.,0.));
#11498=DIRECTION('ref_axis',(1.,0.,0.));
#11499=DIRECTION('center_axis',(0.,1.,0.));
#11500=DIRECTION('ref_axis',(1.,0.,0.));
#11501=DIRECTION('center_axis',(0.,1.,0.));
#11502=DIRECTION('ref_axis',(1.,0.,0.));
#11503=DIRECTION('',(-0.447213595499958,0.894427190999916,-5.47678698264203E-17));
#11504=DIRECTION('center_axis',(0.,-1.,0.));
#11505=DIRECTION('ref_axis',(1.,0.,0.));
#11506=DIRECTION('center_axis',(0.,1.,0.));
#11507=DIRECTION('ref_axis',(1.,0.,0.));
#11508=DIRECTION('',(0.,1.,0.));
#11509=DIRECTION('center_axis',(0.,1.,0.));
#11510=DIRECTION('ref_axis',(1.,0.,0.));
#11511=DIRECTION('center_axis',(0.,-1.,0.));
#11512=DIRECTION('ref_axis',(1.,0.,0.));
#11513=DIRECTION('',(-0.707106781186547,0.707106781186548,-8.65956056235493E-17));
#11514=DIRECTION('center_axis',(0.,-1.,0.));
#11515=DIRECTION('ref_axis',(0.,0.,-1.));
#11516=DIRECTION('center_axis',(0.866025403784439,0.,-0.5));
#11517=DIRECTION('ref_axis',(0.5,0.,0.866025403784439));
#11518=DIRECTION('',(-0.5,0.,-0.866025403784439));
#11519=DIRECTION('',(0.,-1.,0.));
#11520=DIRECTION('',(0.5,0.,0.866025403784439));
#11521=DIRECTION('',(0.,-1.,0.));
#11522=DIRECTION('center_axis',(1.92296268638356E-16,0.,-1.));
#11523=DIRECTION('ref_axis',(1.,0.,1.92296268638356E-16));
#11524=DIRECTION('',(-1.,0.,-1.92296268638356E-16));
#11525=DIRECTION('',(0.,-1.,0.));
#11526=DIRECTION('',(1.,0.,1.92296268638356E-16));
#11527=DIRECTION('center_axis',(-0.866025403784439,0.,-0.5));
#11528=DIRECTION('ref_axis',(0.5,0.,-0.866025403784439));
#11529=DIRECTION('',(-0.5,0.,0.866025403784438));
#11530=DIRECTION('',(0.,-1.,0.));
#11531=DIRECTION('',(0.5,0.,-0.866025403784438));
#11532=DIRECTION('center_axis',(-0.866025403784439,0.,0.5));
#11533=DIRECTION('ref_axis',(-0.5,0.,-0.866025403784439));
#11534=DIRECTION('',(0.5,0.,0.866025403784439));
#11535=DIRECTION('',(0.,-1.,0.));
#11536=DIRECTION('',(-0.5,0.,-0.866025403784439));
#11537=DIRECTION('center_axis',(-1.92296268638356E-16,0.,1.));
#11538=DIRECTION('ref_axis',(-1.,0.,-1.92296268638356E-16));
#11539=DIRECTION('',(1.,0.,1.92296268638356E-16));
#11540=DIRECTION('',(0.,-1.,0.));
#11541=DIRECTION('',(-1.,0.,-1.92296268638356E-16));
#11542=DIRECTION('center_axis',(0.866025403784439,0.,0.5));
#11543=DIRECTION('ref_axis',(-0.5,0.,0.866025403784439));
#11544=DIRECTION('',(0.5,0.,-0.866025403784439));
#11545=DIRECTION('',(-0.5,0.,0.866025403784439));
#11546=DIRECTION('center_axis',(0.,1.,0.));
#11547=DIRECTION('ref_axis',(1.,0.,0.));
#11548=DIRECTION('center_axis',(0.,-1.,0.));
#11549=DIRECTION('ref_axis',(0.,0.,-1.));
#15986=CARTESIAN_POINT('',(0.,0.,0.));
#15987=CARTESIAN_POINT('Origin',(0.45,0.6,0.));
#15988=CARTESIAN_POINT('',(-0.45,0.6,-5.51091059616309E-17));
#15989=CARTESIAN_POINT('Origin',(0.,0.6,0.));
#15990=CARTESIAN_POINT('Origin',(0.,0.575,0.));
#15991=CARTESIAN_POINT('',(-0.5,0.55,-6.12323399573677E-17));
#15992=CARTESIAN_POINT('Origin',(0.,0.55,0.));
#15993=CARTESIAN_POINT('',(-0.475,0.575,-5.81707229594993E-17));
#15994=CARTESIAN_POINT('Origin',(0.,0.29,0.));
#15995=CARTESIAN_POINT('',(-0.5,0.0299999999999998,-6.12323399573677E-17));
#15996=CARTESIAN_POINT('Origin',(0.,0.0299999999999998,0.));
#15997=CARTESIAN_POINT('',(-0.5,0.29,-6.12323399573677E-17));
#15998=CARTESIAN_POINT('Origin',(0.,0.0150000000000001,0.));
#15999=CARTESIAN_POINT('',(-0.47,7.11236625150491E-17,-5.75583995599256E-17));
#16000=CARTESIAN_POINT('Origin',(0.,0.,0.));
#16001=CARTESIAN_POINT('',(-0.485,0.0150000000000001,-5.93953697586466E-17));
#16002=CARTESIAN_POINT('Origin',(0.32,0.,0.));
#16003=CARTESIAN_POINT('',(-0.32,-6.93889390390723E-18,-3.91886975727153E-17));
#16004=CARTESIAN_POINT('Origin',(0.,0.,0.));
#16005=CARTESIAN_POINT('Origin',(0.,-0.02,0.));
#16006=CARTESIAN_POINT('',(-0.2942,-0.0515999999999999,3.60291088309151E-17));
#16007=CARTESIAN_POINT('Origin',(0.,-0.0515999999999999,0.));
#16008=CARTESIAN_POINT('',(-0.31,-0.02,-3.7964050773568E-17));
#16009=CARTESIAN_POINT('Origin',(0.,-1.24,0.));
#16010=CARTESIAN_POINT('',(-0.2942,-2.4458,3.60291088309151E-17));
#16011=CARTESIAN_POINT('Origin',(0.,-2.4458,0.));
#16012=CARTESIAN_POINT('',(-0.2942,-1.24,-3.60291088309151E-17));
#16013=CARTESIAN_POINT('Origin',(0.,-2.47,0.));
#16014=CARTESIAN_POINT('',(-0.24,-2.5,-2.93915231795365E-17));
#16015=CARTESIAN_POINT('Origin',(0.,-2.5,0.));
#16016=CARTESIAN_POINT('',(-0.27,-2.47,-3.30654635769785E-17));
#16017=CARTESIAN_POINT('Origin',(0.,-2.5,0.));
#16018=CARTESIAN_POINT('Origin',(0.144337567297406,-0.6,-0.25));
#16019=CARTESIAN_POINT('',(0.288675134594813,-0.6,0.));
#16020=CARTESIAN_POINT('',(0.144337567297406,-0.6,-0.25));
#16021=CARTESIAN_POINT('',(0.288675134594813,-0.6,0.));
#16022=CARTESIAN_POINT('',(0.144337567297406,-0.96,-0.25));
#16023=CARTESIAN_POINT('',(0.144337567297406,-0.6,-0.25));
#16024=CARTESIAN_POINT('',(0.288675134594813,-0.96,0.));
#16025=CARTESIAN_POINT('',(0.288675134594813,-0.96,0.));
#16026=CARTESIAN_POINT('',(0.288675134594813,-0.6,0.));
#16027=CARTESIAN_POINT('Origin',(-0.144337567297406,-0.6,-0.25));
#16028=CARTESIAN_POINT('',(-0.144337567297406,-0.6,-0.25));
#16029=CARTESIAN_POINT('',(0.144337567297406,-0.6,-0.25));
#16030=CARTESIAN_POINT('',(-0.144337567297406,-0.96,-0.25));
#16031=CARTESIAN_POINT('',(-0.144337567297406,-0.6,-0.25));
#16032=CARTESIAN_POINT('',(0.144337567297406,-0.96,-0.25));
#16033=CARTESIAN_POINT('Origin',(-0.288675134594813,-0.6,-8.32667268468867E-17));
#16034=CARTESIAN_POINT('',(-0.288675134594813,-0.6,-3.53525079574969E-17));
#16035=CARTESIAN_POINT('',(-0.144337567297406,-0.6,-0.25));
#16036=CARTESIAN_POINT('',(-0.288675134594813,-0.96,-5.55111512312578E-17));
#16037=CARTESIAN_POINT('',(-0.288675134594813,-0.6,-3.53525079574969E-17));
#16038=CARTESIAN_POINT('',(-0.144337567297406,-0.96,-0.25));
#16039=CARTESIAN_POINT('Origin',(-0.144337567297407,-0.6,0.25));
#16040=CARTESIAN_POINT('',(-0.144337567297407,-0.6,0.25));
#16041=CARTESIAN_POINT('',(-0.288675134594813,-0.6,-3.53525079574969E-17));
#16042=CARTESIAN_POINT('',(-0.144337567297407,-0.96,0.25));
#16043=CARTESIAN_POINT('',(-0.144337567297407,-0.6,0.25));
#16044=CARTESIAN_POINT('',(-0.288675134594813,-0.96,-3.53525079574969E-17));
#16045=CARTESIAN_POINT('Origin',(0.144337567297406,-0.6,0.25));
#16046=CARTESIAN_POINT('',(0.144337567297406,-0.6,0.25));
#16047=CARTESIAN_POINT('',(-0.144337567297407,-0.6,0.25));
#16048=CARTESIAN_POINT('',(0.144337567297406,-0.96,0.25));
#16049=CARTESIAN_POINT('',(0.144337567297406,-0.6,0.25));
#16050=CARTESIAN_POINT('',(-0.144337567297407,-0.96,0.25));
#16051=CARTESIAN_POINT('Origin',(0.288675134594813,-0.6,0.));
#16052=CARTESIAN_POINT('',(0.144337567297406,-0.6,0.25));
#16053=CARTESIAN_POINT('',(0.144337567297406,-0.96,0.25));
#16054=CARTESIAN_POINT('Origin',(0.,-0.6,0.));
#16055=CARTESIAN_POINT('Origin',(0.,-0.96,0.));
#16974=UNCERTAINTY_MEASURE_WITH_UNIT(LENGTH_MEASURE(0.001),#17047,
'DISTANCE_ACCURACY_VALUE',
'Maximum model space distance between geometric entities at asserted c
onnectivities');
#16993=UNCERTAINTY_MEASURE_WITH_UNIT(LENGTH_MEASURE(0.001),#17047,
'DISTANCE_ACCURACY_VALUE',
'Maximum model space distance between geometric entities at asserted c
onnectivities');
#17027=(
GEOMETRIC_REPRESENTATION_CONTEXT(3)
GLOBAL_UNCERTAINTY_ASSIGNED_CONTEXT((#16974))
GLOBAL_UNIT_ASSIGNED_CONTEXT((#17047,#17049,#17050))
REPRESENTATION_CONTEXT('','3D')
);
#17046=(
GEOMETRIC_REPRESENTATION_CONTEXT(3)
GLOBAL_UNCERTAINTY_ASSIGNED_CONTEXT((#16993))
GLOBAL_UNIT_ASSIGNED_CONTEXT((#17047,#17049,#17050))
REPRESENTATION_CONTEXT('','3D')
);
#17047=(
LENGTH_UNIT()
NAMED_UNIT(*)
SI_UNIT(.CENTI.,.METRE.)
);
#17049=(
NAMED_UNIT(*)
PLANE_ANGLE_UNIT()
SI_UNIT($,.RADIAN.)
);
#17050=(
NAMED_UNIT(*)
SI_UNIT($,.STERADIAN.)
SOLID_ANGLE_UNIT()
);
#17084=SHAPE_DEFINITION_REPRESENTATION(#17141,#17291);
#17141=PRODUCT_DEFINITION_SHAPE('',$,#17344);
#17291=SHAPE_REPRESENTATION('',(#9413),#17027);
#17310=PRODUCT_DEFINITION_CONTEXT('part definition',#17468,'design');
#17344=PRODUCT_DEFINITION('Cap Screw - M6x25','Cap Screw - M6x25',#17396,
#17310);
#17396=PRODUCT_DEFINITION_FORMATION('',$,#17503);
#17468=APPLICATION_CONTEXT(
'Core Data for Automotive Mechanical Design Process');
#17469=PRODUCT_CONTEXT('part definition',#17468,'mechanical');
#17503=PRODUCT('Cap Screw - M6x25','Cap Screw - M6x25',
'Cap Screw - M6x25',(#17469));
#17592=COLOUR_RGB('Black',0.12,0.14,0.17);
#17593=FILL_AREA_STYLE_COLOUR('',#17592);
#17594=FILL_AREA_STYLE('',(#17593));
#17595=SURFACE_STYLE_FILL_AREA(#17594);
#17596=SURFACE_SIDE_STYLE('',(#17595));
#17597=SURFACE_STYLE_USAGE(.BOTH.,#17596);
#17598=PRESENTATION_STYLE_ASSIGNMENT((#17597));
ENDSEC;
END-ISO-10303-21;
